ISO-10303-21;
HEADER;
/* Generated by software containing ST-Developer
 * from STEP Tools, Inc. (www.steptools.com) 
 */

FILE_DESCRIPTION(
/* description */ ('PAT-003'),
/* implementation_level */ '2;1');

FILE_NAME(
/* name */ 'Flat Washer - M5.step',
/* time_stamp */ '2026-10-29T15:45:40-07:00',
/* author */ (''),
/* organization */ (''),
/* preprocessor_version */ 'ST-DEVELOPER v20.2',
/* originating_system */ 'Autodesk Translation Framework v15.17.0.0',
/* authorisation */ '');

FILE_SCHEMA (('AUTOMOTIVE_DESIGN { 1 0 10303 214 3 1 1 }'));
ENDSEC;

DATA;
#10=MECHANICAL_DESIGN_GEOMETRIC_PRESENTATION_REPRESENTATION('',(#149),#5761);
#109=CONICAL_SURFACE('',#3520,0.275,0.785398163397449);
#125=SHAPE_REPRESENTATION_RELATIONSHIP('SRR','None',#5819,#137);
#137=ADVANCED_BREP_SHAPE_REPRESENTATION('',(#161),#5750);
#149=STYLED_ITEM('',(#5956),#161);
#161=MANIFOLD_SOLID_BREP('Body1',#3323);
#179=FACE_BOUND('',#570,.T.);
#180=FACE_BOUND('',#573,.T.);
#228=PLANE('',#3525);
#229=PLANE('',#3529);
#370=FACE_OUTER_BOUND('',#567,.T.);
#371=FACE_OUTER_BOUND('',#568,.T.);
#372=FACE_OUTER_BOUND('',#569,.T.);
#373=FACE_OUTER_BOUND('',#571,.T.);
#374=FACE_OUTER_BOUND('',#572,.T.);
#567=EDGE_LOOP('',(#2356,#2357,#2358,#2359));
#568=EDGE_LOOP('',(#2360,#2361,#2362,#2363));
#569=EDGE_LOOP('',(#2364));
#570=EDGE_LOOP('',(#2365));
#571=EDGE_LOOP('',(#2366,#2367,#2368,#2369));
#572=EDGE_LOOP('',(#2370));
#573=EDGE_LOOP('',(#2371));
#803=LINE('',#4900,#1125);
#804=LINE('',#4904,#1126);
#805=LINE('',#4911,#1127);
#1125=VECTOR('',#3946,0.275);
#1126=VECTOR('',#3951,0.265);
#1127=VECTOR('',#3960,0.5);
#1412=CIRCLE('',#3521,0.285);
#1413=CIRCLE('',#3522,0.265);
#1414=CIRCLE('',#3524,0.265);
#1415=CIRCLE('',#3526,0.5);
#1416=CIRCLE('',#3528,0.5);
#1538=VERTEX_POINT('',#4897);
#1539=VERTEX_POINT('',#4899);
#1540=VERTEX_POINT('',#4903);
#1541=VERTEX_POINT('',#4907);
#1542=VERTEX_POINT('',#4910);
#1849=EDGE_CURVE('',#1538,#1538,#1412,.T.);
#1850=EDGE_CURVE('',#1538,#1539,#803,.T.);
#1851=EDGE_CURVE('',#1539,#1539,#1413,.T.);
#1852=EDGE_CURVE('',#1539,#1540,#804,.T.);
#1853=EDGE_CURVE('',#1540,#1540,#1414,.T.);
#1854=EDGE_CURVE('',#1541,#1541,#1415,.T.);
#1855=EDGE_CURVE('',#1541,#1542,#805,.T.);
#1856=EDGE_CURVE('',#1542,#1542,#1416,.T.);
#2356=ORIENTED_EDGE('',*,*,#1849,.T.);
#2357=ORIENTED_EDGE('',*,*,#1850,.T.);
#2358=ORIENTED_EDGE('',*,*,#1851,.T.);
#2359=ORIENTED_EDGE('',*,*,#1850,.F.);
#2360=ORIENTED_EDGE('',*,*,#1851,.F.);
#2361=ORIENTED_EDGE('',*,*,#1852,.T.);
#2362=ORIENTED_EDGE('',*,*,#1853,.T.);
#2363=ORIENTED_EDGE('',*,*,#1852,.F.);
#2364=ORIENTED_EDGE('',*,*,#1854,.T.);
#2365=ORIENTED_EDGE('',*,*,#1849,.F.);
#2366=ORIENTED_EDGE('',*,*,#1854,.F.);
#2367=ORIENTED_EDGE('',*,*,#1855,.T.);
#2368=ORIENTED_EDGE('',*,*,#1856,.T.);
#2369=ORIENTED_EDGE('',*,*,#1855,.F.);
#2370=ORIENTED_EDGE('',*,*,#1856,.F.);
#2371=ORIENTED_EDGE('',*,*,#1853,.F.);
#3101=CYLINDRICAL_SURFACE('',#3523,0.265);
#3102=CYLINDRICAL_SURFACE('',#3527,0.5);
#3163=ADVANCED_FACE('',(#370),#109,.F.);
#3164=ADVANCED_FACE('',(#371),#3101,.F.);
#3165=ADVANCED_FACE('',(#372,#179),#228,.T.);
#3166=ADVANCED_FACE('',(#373),#3102,.T.);
#3167=ADVANCED_FACE('',(#374,#180),#229,.F.);
#3323=CLOSED_SHELL('',(#3163,#3164,#3165,#3166,#3167));
#3519=AXIS2_PLACEMENT_3D('',#4895,#3940,#3941);
#3520=AXIS2_PLACEMENT_3D('',#4896,#3942,#3943);
#3521=AXIS2_PLACEMENT_3D('',#4898,#3944,#3945);
#3522=AXIS2_PLACEMENT_3D('',#4901,#3947,#3948);
#3523=AXIS2_PLACEMENT_3D('',#4902,#3949,#3950);
#3524=AXIS2_PLACEMENT_3D('',#4905,#3952,#3953);
#3525=AXIS2_PLACEMENT_3D('',#4906,#3954,#3955);
#3526=AXIS2_PLACEMENT_3D('',#4908,#3956,#3957);
#3527=AXIS2_PLACEMENT_3D('',#4909,#3958,#3959);
#3528=AXIS2_PLACEMENT_3D('',#4912,#3961,#3962);
#3529=AXIS2_PLACEMENT_3D('',#4913,#3963,#3964);
#3940=DIRECTION('axis',(0.,0.,1.));
#3941=DIRECTION('refdir',(1.,0.,0.));
#3942=DIRECTION('center_axis',(0.,1.,0.));
#3943=DIRECTION('ref_axis',(1.,0.,0.));
#3944=DIRECTION('center_axis',(0.,1.,0.));
#3945=DIRECTION('ref_axis',(1.,0.,0.));
#3946=DIRECTION('',(0.707106781186548,-0.707106781186547,-8.65956056235494E-17));
#3947=DIRECTION('center_axis',(0.,-1.,0.));
#3948=DIRECTION('ref_axis',(1.,0.,0.));
#3949=DIRECTION('center_axis',(0.,1.,0.));
#3950=DIRECTION('ref_axis',(1.,0.,0.));
#3951=DIRECTION('',(0.,-1.,0.));
#3952=DIRECTION('center_axis',(0.,-1.,0.));
#3953=DIRECTION('ref_axis',(1.,0.,0.));
#3954=DIRECTION('center_axis',(0.,1.,0.));
#3955=DIRECTION('ref_axis',(1.,0.,0.));
#3956=DIRECTION('center_axis',(0.,1.,0.));
#3957=DIRECTION('ref_axis',(1.,0.,0.));
#3958=DIRECTION('center_axis',(0.,1.,0.));
#3959=DIRECTION('ref_axis',(1.,0.,0.));
#3960=DIRECTION('',(0.,-1.,0.));
#3961=DIRECTION('center_axis',(0.,1.,0.));
#3962=DIRECTION('ref_axis',(1.,0.,0.));
#3963=DIRECTION('center_axis',(0.,1.,0.));
#3964=DIRECTION('ref_axis',(1.,0.,0.));
#4895=CARTESIAN_POINT('',(0.,0.,0.));
#4896=CARTESIAN_POINT('Origin',(0.,0.09,0.));
#4897=CARTESIAN_POINT('',(-0.285,0.1,3.49024337756996E-17));
#4898=CARTESIAN_POINT('Origin',(0.,0.1,0.));
#4899=CARTESIAN_POINT('',(-0.265,0.08,-3.24531401774049E-17));
#4900=CARTESIAN_POINT('',(-0.275,0.09,3.36777869765522E-17));
#4901=CARTESIAN_POINT('Origin',(0.,0.08,0.));
#4902=CARTESIAN_POINT('Origin',(0.,0.,0.));
#4903=CARTESIAN_POINT('',(-0.265,0.,3.24531401774049E-17));
#4904=CARTESIAN_POINT('',(-0.265,0.,3.24531401774049E-17));
#4905=CARTESIAN_POINT('Origin',(0.,0.,0.));
#4906=CARTESIAN_POINT('Origin',(0.,0.1,0.));
#4907=CARTESIAN_POINT('',(-0.5,0.1,6.12323399573677E-17));
#4908=CARTESIAN_POINT('Origin',(0.,0.1,0.));
#4909=CARTESIAN_POINT('Origin',(0.,0.,0.));
#4910=CARTESIAN_POINT('',(-0.5,0.,6.12323399573677E-17));
#4911=CARTESIAN_POINT('',(-0.5,0.,6.12323399573677E-17));
#4912=CARTESIAN_POINT('Origin',(0.,0.,0.));
#4913=CARTESIAN_POINT('Origin',(0.,0.,0.));
#5734=UNCERTAINTY_MEASURE_WITH_UNIT(LENGTH_MEASURE(0.001),#5762,
'DISTANCE_ACCURACY_VALUE',
'Maximum model space distance between geometric entities at asserted c
onnectivities');
#5745=UNCERTAINTY_MEASURE_WITH_UNIT(LENGTH_MEASURE(0.001),#5762,
'DISTANCE_ACCURACY_VALUE',
'Maximum model space distance between geometric entities at asserted c
onnectivities');
#5750=(
GEOMETRIC_REPRESENTATION_CONTEXT(3)
GLOBAL_UNCERTAINTY_ASSIGNED_CONTEXT((#5734))
GLOBAL_UNIT_ASSIGNED_CONTEXT((#5762,#5764,#5765))
REPRESENTATION_CONTEXT('','3D')
);
#5761=(
GEOMETRIC_REPRESENTATION_CONTEXT(3)
GLOBAL_UNCERTAINTY_ASSIGNED_CONTEXT((#5745))
GLOBAL_UNIT_ASSIGNED_CONTEXT((#5762,#5764,#5765))
REPRESENTATION_CONTEXT('','3D')
);
#5762=(
LENGTH_UNIT()
NAMED_UNIT(*)
SI_UNIT(.CENTI.,.METRE.)
);
#5764=(
NAMED_UNIT(*)
PLANE_ANGLE_UNIT()
SI_UNIT($,.RADIAN.)
);
#5765=(
NAMED_UNIT(*)
SI_UNIT($,.STERADIAN.)
SOLID_ANGLE_UNIT()
);
#5770=SHAPE_DEFINITION_REPRESENTATION(#5785,#5819);
#5785=PRODUCT_DEFINITION_SHAPE('',$,#5835);
#5819=SHAPE_REPRESENTATION('',(#3519),#5750);
#5830=PRODUCT_DEFINITION_CONTEXT('part definition',#5877,'design');
#5835=PRODUCT_DEFINITION('Flat Washer - M5','Flat Washer - M5',#5850,#5830);
#5850=PRODUCT_DEFINITION_FORMATION('',$,#5883);
#5877=APPLICATION_CONTEXT(
'Core Data for Automotive Mechanical Design Process');
#5878=PRODUCT_CONTEXT('part definition',#5877,'mechanical');
#5883=PRODUCT('Flat Washer - M5','Flat Washer - M5','Flat Washer - M5',
(#5878));
#5950=COLOUR_RGB('Black',0.12,0.14,0.17);
#5951=FILL_AREA_STYLE_COLOUR('',#5950);
#5952=FILL_AREA_STYLE('',(#5951));
#5953=SURFACE_STYLE_FILL_AREA(#5952);
#5954=SURFACE_SIDE_STYLE('',(#5953));
#5955=SURFACE_STYLE_USAGE(.BOTH.,#5954);
#5956=PRESENTATION_STYLE_ASSIGNMENT((#5955));
ENDSEC;
END-ISO-10303-21;
